ISO-10303-21;
HEADER;
/* Generated by software containing ST-Developer
 * from STEP Tools, Inc. (www.steptools.com) 
 */

FILE_DESCRIPTION(
/* description */ ('PAT-091'),
/* implementation_level */ '2;1');

FILE_NAME(
/* name */ 'M4 low-profile retaining screw (3).step',
/* time_stamp */ '2026-10-27T15:34:44-07:00',
/* author */ (''),
/* organization */ (''),
/* preprocessor_version */ 'ST-DEVELOPER v20.2',
/* originating_system */ 'Autodesk Translation Framework v15.17.0.0',
/* authorisation */ '');

FILE_SCHEMA (('AUTOMOTIVE_DESIGN { 1 0 10303 214 3 1 1 }'));
ENDSEC;

DATA;
#10=MECHANICAL_DESIGN_GEOMETRIC_PRESENTATION_REPRESENTATION('',(#1051),#25100);
#831=SHAPE_REPRESENTATION_RELATIONSHIP('SRR','None',#25598,#941);
#941=ADVANCED_BREP_SHAPE_REPRESENTATION('',(#1172),#25068);
#1051=STYLED_ITEM('',(#26198),#1172);
#1172=MANIFOLD_SOLID_BREP('Body1',#13331);
#1556=FACE_BOUND('',#3821,.T.);
#1969=PLANE('',#15882);
#1970=PLANE('',#15887);
#1971=PLANE('',#15890);
#2661=FACE_OUTER_BOUND('',#3820,.T.);
#2662=FACE_OUTER_BOUND('',#3822,.T.);
#2663=FACE_OUTER_BOUND('',#3823,.T.);
#2664=FACE_OUTER_BOUND('',#3824,.T.);
#2665=FACE_OUTER_BOUND('',#3825,.T.);
#3820=EDGE_LOOP('',(#11330));
#3821=EDGE_LOOP('',(#11331));
#3822=EDGE_LOOP('',(#11332,#11333,#11334,#11335));
#3823=EDGE_LOOP('',(#11336));
#3824=EDGE_LOOP('',(#11337,#11338,#11339,#11340));
#3825=EDGE_LOOP('',(#11341));
#4763=LINE('',#23755,#5503);
#4764=LINE('',#23761,#5504);
#5503=VECTOR('',#19709,0.350000000000001);
#5504=VECTOR('',#19718,0.199999999999999);
#6140=CIRCLE('',#15883,0.350000000000001);
#6141=CIRCLE('',#15884,0.199999999999999);
#6142=CIRCLE('',#15886,0.350000000000001);
#6143=CIRCLE('',#15889,0.199999999999999);
#7165=VERTEX_POINT('',#23749);
#7166=VERTEX_POINT('',#23751);
#7167=VERTEX_POINT('',#23754);
#7168=VERTEX_POINT('',#23759);
#8600=EDGE_CURVE('',#7165,#7165,#6140,.T.);
#8601=EDGE_CURVE('',#7166,#7166,#6141,.T.);
#8602=EDGE_CURVE('',#7165,#7167,#4763,.T.);
#8603=EDGE_CURVE('',#7167,#7167,#6142,.T.);
#8604=EDGE_CURVE('',#7168,#7168,#6143,.T.);
#8605=EDGE_CURVE('',#7168,#7166,#4764,.T.);
#11330=ORIENTED_EDGE('',*,*,#8600,.T.);
#11331=ORIENTED_EDGE('',*,*,#8601,.F.);
#11332=ORIENTED_EDGE('',*,*,#8600,.F.);
#11333=ORIENTED_EDGE('',*,*,#8602,.T.);
#11334=ORIENTED_EDGE('',*,*,#8603,.T.);
#11335=ORIENTED_EDGE('',*,*,#8602,.F.);
#11336=ORIENTED_EDGE('',*,*,#8603,.F.);
#11337=ORIENTED_EDGE('',*,*,#8604,.F.);
#11338=ORIENTED_EDGE('',*,*,#8605,.T.);
#11339=ORIENTED_EDGE('',*,*,#8601,.T.);
#11340=ORIENTED_EDGE('',*,*,#8605,.F.);
#11341=ORIENTED_EDGE('',*,*,#8604,.T.);
#12331=CYLINDRICAL_SURFACE('',#15885,0.350000000000001);
#12332=CYLINDRICAL_SURFACE('',#15888,0.199999999999999);
#13028=ADVANCED_FACE('',(#2661,#1556),#1969,.T.);
#13029=ADVANCED_FACE('',(#2662),#12331,.T.);
#13030=ADVANCED_FACE('',(#2663),#1970,.F.);
#13031=ADVANCED_FACE('',(#2664),#12332,.T.);
#13032=ADVANCED_FACE('',(#2665),#1971,.T.);
#13331=CLOSED_SHELL('',(#13028,#13029,#13030,#13031,#13032));
#15881=AXIS2_PLACEMENT_3D('',#23747,#19699,#19700);
#15882=AXIS2_PLACEMENT_3D('',#23748,#19701,#19702);
#15883=AXIS2_PLACEMENT_3D('',#23750,#19703,#19704);
#15884=AXIS2_PLACEMENT_3D('',#23752,#19705,#19706);
#15885=AXIS2_PLACEMENT_3D('',#23753,#19707,#19708);
#15886=AXIS2_PLACEMENT_3D('',#23756,#19710,#19711);
#15887=AXIS2_PLACEMENT_3D('',#23757,#19712,#19713);
#15888=AXIS2_PLACEMENT_3D('',#23758,#19714,#19715);
#15889=AXIS2_PLACEMENT_3D('',#23760,#19716,#19717);
#15890=AXIS2_PLACEMENT_3D('',#23762,#19719,#19720);
#19699=DIRECTION('axis',(0.,0.,1.));
#19700=DIRECTION('refdir',(1.,0.,0.));
#19701=DIRECTION('center_axis',(0.,1.,0.));
#19702=DIRECTION('ref_axis',(1.,0.,0.));
#19703=DIRECTION('center_axis',(0.,1.,0.));
#19704=DIRECTION('ref_axis',(1.,0.,0.));
#19705=DIRECTION('center_axis',(0.,1.,0.));
#19706=DIRECTION('ref_axis',(1.,0.,0.));
#19707=DIRECTION('center_axis',(0.,1.,0.));
#19708=DIRECTION('ref_axis',(1.,0.,0.));
#19709=DIRECTION('',(0.,-1.,0.));
#19710=DIRECTION('center_axis',(0.,1.,0.));
#19711=DIRECTION('ref_axis',(1.,0.,0.));
#19712=DIRECTION('center_axis',(0.,1.,0.));
#19713=DIRECTION('ref_axis',(1.,0.,0.));
#19714=DIRECTION('center_axis',(0.,1.,0.));
#19715=DIRECTION('ref_axis',(1.,0.,0.));
#19716=DIRECTION('center_axis',(0.,1.,0.));
#19717=DIRECTION('ref_axis',(1.,0.,0.));
#19718=DIRECTION('',(0.,-1.,0.));
#19719=DIRECTION('center_axis',(0.,1.,0.));
#19720=DIRECTION('ref_axis',(1.,0.,0.));
#23747=CARTESIAN_POINT('',(0.,0.,0.));
#23748=CARTESIAN_POINT('Origin',(20.6730642762322,-5.8,6.69185245480489));
#23749=CARTESIAN_POINT('',(20.3230642762322,-5.8,6.69185245480489));
#23750=CARTESIAN_POINT('Origin',(20.6730642762322,-5.8,6.69185245480489));
#23751=CARTESIAN_POINT('',(20.4730642762322,-5.8,6.69185245480489));
#23752=CARTESIAN_POINT('Origin',(20.6730642762322,-5.8,6.69185245480489));
#23753=CARTESIAN_POINT('Origin',(20.6730642762322,-5.9,6.69185245480489));
#23754=CARTESIAN_POINT('',(20.3230642762322,-5.9,6.69185245480489));
#23755=CARTESIAN_POINT('',(20.3230642762322,-5.9,6.69185245480489));
#23756=CARTESIAN_POINT('Origin',(20.6730642762322,-5.9,6.69185245480489));
#23757=CARTESIAN_POINT('Origin',(20.6730642762322,-5.9,6.69185245480489));
#23758=CARTESIAN_POINT('Origin',(20.6730642762322,-5.8,6.69185245480489));
#23759=CARTESIAN_POINT('',(20.4730642762322,-5.1,6.69185245480489));
#23760=CARTESIAN_POINT('Origin',(20.6730642762322,-5.1,6.69185245480489));
#23761=CARTESIAN_POINT('',(20.4730642762322,-5.8,6.69185245480489));
#23762=CARTESIAN_POINT('Origin',(20.6730642762322,-5.1,6.69185245480489));
#24947=UNCERTAINTY_MEASURE_WITH_UNIT(LENGTH_MEASURE(0.001),#25101,
'DISTANCE_ACCURACY_VALUE',
'Maximum model space distance between geometric entities at asserted c
onnectivities');
#24979=UNCERTAINTY_MEASURE_WITH_UNIT(LENGTH_MEASURE(0.001),#25101,
'DISTANCE_ACCURACY_VALUE',
'Maximum model space distance between geometric entities at asserted c
onnectivities');
#25068=(
GEOMETRIC_REPRESENTATION_CONTEXT(3)
GLOBAL_UNCERTAINTY_ASSIGNED_CONTEXT((#24947))
GLOBAL_UNIT_ASSIGNED_CONTEXT((#25101,#25103,#25104))
REPRESENTATION_CONTEXT('','3D')
);
#25100=(
GEOMETRIC_REPRESENTATION_CONTEXT(3)
GLOBAL_UNCERTAINTY_ASSIGNED_CONTEXT((#24979))
GLOBAL_UNIT_ASSIGNED_CONTEXT((#25101,#25103,#25104))
REPRESENTATION_CONTEXT('','3D')
);
#25101=(
LENGTH_UNIT()
NAMED_UNIT(*)
SI_UNIT(.CENTI.,.METRE.)
);
#25103=(
NAMED_UNIT(*)
PLANE_ANGLE_UNIT()
SI_UNIT($,.RADIAN.)
);
#25104=(
NAMED_UNIT(*)
SI_UNIT($,.STERADIAN.)
SOLID_ANGLE_UNIT()
);
#25193=SHAPE_DEFINITION_REPRESENTATION(#25387,#25598);
#25387=PRODUCT_DEFINITION_SHAPE('',$,#25719);
#25598=SHAPE_REPRESENTATION('',(#15881),#25068);
#25630=PRODUCT_DEFINITION_CONTEXT('part definition',#25992,'design');
#25719=PRODUCT_DEFINITION('M4 low-profile retaining screw (3)',
'M4 low-profile retaining screw (3)',#25839,#25630);
#25839=PRODUCT_DEFINITION_FORMATION('',$,#26082);
#25992=APPLICATION_CONTEXT(
'Core Data for Automotive Mechanical Design Process');
#25993=PRODUCT_CONTEXT('part definition',#25992,'mechanical');
#26082=PRODUCT('M4 low-profile retaining screw (3)',
'M4 low-profile retaining screw (3)','M4 low-profile retaining screw (3)',(#25993));
#26192=COLOUR_RGB('Black',0.12,0.14,0.17);
#26193=FILL_AREA_STYLE_COLOUR('',#26192);
#26194=FILL_AREA_STYLE('',(#26193));
#26195=SURFACE_STYLE_FILL_AREA(#26194);
#26196=SURFACE_SIDE_STYLE('',(#26195));
#26197=SURFACE_STYLE_USAGE(.BOTH.,#26196);
#26198=PRESENTATION_STYLE_ASSIGNMENT((#26197));
ENDSEC;
END-ISO-10303-21;
